ISO-10303-21;
HEADER;
/* Generated by software containing ST-Developer
 * from STEP Tools, Inc. (www.steptools.com) 
 */

FILE_DESCRIPTION(
/* description */ ('Hand-crank gear train demonstrator'),
/* implementation_level */ '2;1');

FILE_NAME(
/* name */ 'M6x18 mounting screw.step',
/* time_stamp */ '2026-10-28T03:22:13-07:00',
/* author */ (''),
/* organization */ (''),
/* preprocessor_version */ 'ST-DEVELOPER v20.2',
/* originating_system */ 'Autodesk Translation Framework v15.17.0.0',
/* authorisation */ '');

FILE_SCHEMA (('AUTOMOTIVE_DESIGN { 1 0 10303 214 3 1 1 }'));
ENDSEC;

DATA;
#10=MECHANICAL_DESIGN_GEOMETRIC_PRESENTATION_REPRESENTATION('',(#1195),#62758);
#1025=CONICAL_SURFACE('',#17373,0.475,0.785398163397449);
#1026=CONICAL_SURFACE('',#17377,0.485,0.785398163397448);
#1027=CONICAL_SURFACE('',#17381,0.31,0.463647609000806);
#1051=ORIENTED_CLOSED_SHELL('',*,#16375,.F.);
#1056=BREP_WITH_VOIDS('Body1',#16376,(#1051));
#1067=SHAPE_REPRESENTATION_RELATIONSHIP('SRR','None',#63039,#1131);
#1131=ADVANCED_BREP_SHAPE_REPRESENTATION('',(#1056),#62693);
#1195=STYLED_ITEM('',(#63469),#1056);
#1442=FACE_BOUND('',#3255,.T.);
#1659=PLANE('',#17361);
#1660=PLANE('',#17362);
#1661=PLANE('',#17363);
#1662=PLANE('',#17364);
#1663=PLANE('',#17365);
#1664=PLANE('',#17366);
#1665=PLANE('',#17367);
#1666=PLANE('',#17368);
#1667=PLANE('',#17369);
#1668=PLANE('',#17371);
#1669=PLANE('',#17379);
#2205=FACE_OUTER_BOUND('',#3241,.T.);
#2206=FACE_OUTER_BOUND('',#3242,.T.);
#2207=FACE_OUTER_BOUND('',#3243,.T.);
#2208=FACE_OUTER_BOUND('',#3244,.T.);
#2209=FACE_OUTER_BOUND('',#3245,.T.);
#2210=FACE_OUTER_BOUND('',#3246,.T.);
#2211=FACE_OUTER_BOUND('',#3247,.T.);
#2212=FACE_OUTER_BOUND('',#3248,.T.);
#2213=FACE_OUTER_BOUND('',#3249,.T.);
#2214=FACE_OUTER_BOUND('',#3250,.T.);
#2215=FACE_OUTER_BOUND('',#3251,.T.);
#2216=FACE_OUTER_BOUND('',#3252,.T.);
#2217=FACE_OUTER_BOUND('',#3253,.T.);
#2218=FACE_OUTER_BOUND('',#3254,.T.);
#2219=FACE_OUTER_BOUND('',#3256,.T.);
#2220=FACE_OUTER_BOUND('',#3257,.T.);
#3241=EDGE_LOOP('',(#11231,#11232,#11233,#11234));
#3242=EDGE_LOOP('',(#11235,#11236,#11237,#11238));
#3243=EDGE_LOOP('',(#11239,#11240,#11241,#11242));
#3244=EDGE_LOOP('',(#11243,#11244,#11245,#11246));
#3245=EDGE_LOOP('',(#11247,#11248,#11249,#11250));
#3246=EDGE_LOOP('',(#11251,#11252,#11253,#11254));
#3247=EDGE_LOOP('',(#11255,#11256,#11257,#11258,#11259,#11260));
#3248=EDGE_LOOP('',(#11261,#11262,#11263,#11264,#11265,#11266));
#3249=EDGE_LOOP('',(#11267));
#3250=EDGE_LOOP('',(#11268));
#3251=EDGE_LOOP('',(#11269,#11270,#11271,#11272));
#3252=EDGE_LOOP('',(#11273,#11274,#11275,#11276));
#3253=EDGE_LOOP('',(#11277,#11278,#11279,#11280));
#3254=EDGE_LOOP('',(#11281));
#3255=EDGE_LOOP('',(#11282));
#3256=EDGE_LOOP('',(#11283,#11284,#11285,#11286));
#3257=EDGE_LOOP('',(#11287,#11288,#11289,#11290));
#4372=LINE('',#23733,#5504);
#4373=LINE('',#23735,#5505);
#4374=LINE('',#23737,#5506);
#4375=LINE('',#23738,#5507);
#4376=LINE('',#23741,#5508);
#4377=LINE('',#23743,#5509);
#4378=LINE('',#23744,#5510);
#4379=LINE('',#23747,#5511);
#4380=LINE('',#23749,#5512);
#4381=LINE('',#23750,#5513);
#4382=LINE('',#23753,#5514);
#4383=LINE('',#23755,#5515);
#4384=LINE('',#23756,#5516);
#4385=LINE('',#23759,#5517);
#4386=LINE('',#23761,#5518);
#4387=LINE('',#23762,#5519);
#4388=LINE('',#23764,#5520);
#4389=LINE('',#23765,#5521);
#4390=LINE('',#23777,#5522);
#4391=LINE('',#23781,#5523);
#4392=LINE('',#23785,#5524);
#4393=LINE('',#23792,#5525);
#4394=LINE('',#23794,#5526);
#5504=VECTOR('',#19325,1.);
#5505=VECTOR('',#19326,1.);
#5506=VECTOR('',#19327,1.);
#5507=VECTOR('',#19328,1.);
#5508=VECTOR('',#19331,1.);
#5509=VECTOR('',#19332,1.);
#5510=VECTOR('',#19333,1.);
#5511=VECTOR('',#19336,1.);
#5512=VECTOR('',#19337,1.);
#5513=VECTOR('',#19338,1.);
#5514=VECTOR('',#19341,1.);
#5515=VECTOR('',#19342,1.);
#5516=VECTOR('',#19343,1.);
#5517=VECTOR('',#19346,1.);
#5518=VECTOR('',#19347,1.);
#5519=VECTOR('',#19348,1.);
#5520=VECTOR('',#19351,1.);
#5521=VECTOR('',#19352,1.);
#5522=VECTOR('',#19369,0.475);
#5523=VECTOR('',#19374,0.5);
#5524=VECTOR('',#19379,0.485);
#5525=VECTOR('',#19388,0.31);
#5526=VECTOR('',#19391,0.3);
#6662=CIRCLE('',#17370,0.2942);
#6663=CIRCLE('',#17372,0.45);
#6664=CIRCLE('',#17374,0.5);
#6665=CIRCLE('',#17376,0.5);
#6666=CIRCLE('',#17378,0.47);
#6667=CIRCLE('',#17380,0.32);
#6668=CIRCLE('',#17382,0.2942);
#7344=VERTEX_POINT('',#23731);
#7345=VERTEX_POINT('',#23732);
#7346=VERTEX_POINT('',#23734);
#7347=VERTEX_POINT('',#23736);
#7348=VERTEX_POINT('',#23740);
#7349=VERTEX_POINT('',#23742);
#7350=VERTEX_POINT('',#23746);
#7351=VERTEX_POINT('',#23748);
#7352=VERTEX_POINT('',#23752);
#7353=VERTEX_POINT('',#23754);
#7354=VERTEX_POINT('',#23758);
#7355=VERTEX_POINT('',#23760);
#7356=VERTEX_POINT('',#23769);
#7357=VERTEX_POINT('',#23772);
#7358=VERTEX_POINT('',#23775);
#7359=VERTEX_POINT('',#23779);
#7360=VERTEX_POINT('',#23783);
#7361=VERTEX_POINT('',#23787);
#7362=VERTEX_POINT('',#23790);
#8867=EDGE_CURVE('',#7344,#7345,#4372,.T.);
#8868=EDGE_CURVE('',#7345,#7346,#4373,.T.);
#8869=EDGE_CURVE('',#7346,#7347,#4374,.T.);
#8870=EDGE_CURVE('',#7344,#7347,#4375,.T.);
#8871=EDGE_CURVE('',#7345,#7348,#4376,.T.);
#8872=EDGE_CURVE('',#7348,#7349,#4377,.T.);
#8873=EDGE_CURVE('',#7349,#7346,#4378,.T.);
#8874=EDGE_CURVE('',#7348,#7350,#4379,.T.);
#8875=EDGE_CURVE('',#7350,#7351,#4380,.T.);
#8876=EDGE_CURVE('',#7351,#7349,#4381,.T.);
#8877=EDGE_CURVE('',#7350,#7352,#4382,.T.);
#8878=EDGE_CURVE('',#7352,#7353,#4383,.T.);
#8879=EDGE_CURVE('',#7353,#7351,#4384,.T.);
#8880=EDGE_CURVE('',#7352,#7354,#4385,.T.);
#8881=EDGE_CURVE('',#7354,#7355,#4386,.T.);
#8882=EDGE_CURVE('',#7355,#7353,#4387,.T.);
#8883=EDGE_CURVE('',#7354,#7344,#4388,.T.);
#8884=EDGE_CURVE('',#7347,#7355,#4389,.T.);
#8885=EDGE_CURVE('',#7356,#7356,#6662,.T.);
#8886=EDGE_CURVE('',#7357,#7357,#6663,.T.);
#8887=EDGE_CURVE('',#7358,#7358,#6664,.T.);
#8888=EDGE_CURVE('',#7358,#7357,#4390,.T.);
#8889=EDGE_CURVE('',#7359,#7359,#6665,.T.);
#8890=EDGE_CURVE('',#7359,#7358,#4391,.T.);
#8891=EDGE_CURVE('',#7360,#7360,#6666,.T.);
#8892=EDGE_CURVE('',#7360,#7359,#4392,.T.);
#8893=EDGE_CURVE('',#7361,#7361,#6667,.T.);
#8894=EDGE_CURVE('',#7362,#7362,#6668,.F.);
#8895=EDGE_CURVE('',#7362,#7361,#4393,.T.);
#8896=EDGE_CURVE('',#7356,#7362,#4394,.T.);
#11231=ORIENTED_EDGE('',*,*,#8867,.T.);
#11232=ORIENTED_EDGE('',*,*,#8868,.T.);
#11233=ORIENTED_EDGE('',*,*,#8869,.T.);
#11234=ORIENTED_EDGE('',*,*,#8870,.F.);
#11235=ORIENTED_EDGE('',*,*,#8871,.T.);
#11236=ORIENTED_EDGE('',*,*,#8872,.T.);
#11237=ORIENTED_EDGE('',*,*,#8873,.T.);
#11238=ORIENTED_EDGE('',*,*,#8868,.F.);
#11239=ORIENTED_EDGE('',*,*,#8874,.T.);
#11240=ORIENTED_EDGE('',*,*,#8875,.T.);
#11241=ORIENTED_EDGE('',*,*,#8876,.T.);
#11242=ORIENTED_EDGE('',*,*,#8872,.F.);
#11243=ORIENTED_EDGE('',*,*,#8877,.T.);
#11244=ORIENTED_EDGE('',*,*,#8878,.T.);
#11245=ORIENTED_EDGE('',*,*,#8879,.T.);
#11246=ORIENTED_EDGE('',*,*,#8875,.F.);
#11247=ORIENTED_EDGE('',*,*,#8880,.T.);
#11248=ORIENTED_EDGE('',*,*,#8881,.T.);
#11249=ORIENTED_EDGE('',*,*,#8882,.T.);
#11250=ORIENTED_EDGE('',*,*,#8878,.F.);
#11251=ORIENTED_EDGE('',*,*,#8883,.T.);
#11252=ORIENTED_EDGE('',*,*,#8870,.T.);
#11253=ORIENTED_EDGE('',*,*,#8884,.T.);
#11254=ORIENTED_EDGE('',*,*,#8881,.F.);
#11255=ORIENTED_EDGE('',*,*,#8883,.F.);
#11256=ORIENTED_EDGE('',*,*,#8880,.F.);
#11257=ORIENTED_EDGE('',*,*,#8877,.F.);
#11258=ORIENTED_EDGE('',*,*,#8874,.F.);
#11259=ORIENTED_EDGE('',*,*,#8871,.F.);
#11260=ORIENTED_EDGE('',*,*,#8867,.F.);
#11261=ORIENTED_EDGE('',*,*,#8884,.F.);
#11262=ORIENTED_EDGE('',*,*,#8869,.F.);
#11263=ORIENTED_EDGE('',*,*,#8873,.F.);
#11264=ORIENTED_EDGE('',*,*,#8876,.F.);
#11265=ORIENTED_EDGE('',*,*,#8879,.F.);
#11266=ORIENTED_EDGE('',*,*,#8882,.F.);
#11267=ORIENTED_EDGE('',*,*,#8885,.F.);
#11268=ORIENTED_EDGE('',*,*,#8886,.F.);
#11269=ORIENTED_EDGE('',*,*,#8887,.F.);
#11270=ORIENTED_EDGE('',*,*,#8888,.T.);
#11271=ORIENTED_EDGE('',*,*,#8886,.T.);
#11272=ORIENTED_EDGE('',*,*,#8888,.F.);
#11273=ORIENTED_EDGE('',*,*,#8889,.F.);
#11274=ORIENTED_EDGE('',*,*,#8890,.T.);
#11275=ORIENTED_EDGE('',*,*,#8887,.T.);
#11276=ORIENTED_EDGE('',*,*,#8890,.F.);
#11277=ORIENTED_EDGE('',*,*,#8891,.F.);
#11278=ORIENTED_EDGE('',*,*,#8892,.T.);
#11279=ORIENTED_EDGE('',*,*,#8889,.T.);
#11280=ORIENTED_EDGE('',*,*,#8892,.F.);
#11281=ORIENTED_EDGE('',*,*,#8891,.T.);
#11282=ORIENTED_EDGE('',*,*,#8893,.F.);
#11283=ORIENTED_EDGE('',*,*,#8894,.F.);
#11284=ORIENTED_EDGE('',*,*,#8895,.T.);
#11285=ORIENTED_EDGE('',*,*,#8893,.T.);
#11286=ORIENTED_EDGE('',*,*,#8895,.F.);
#11287=ORIENTED_EDGE('',*,*,#8885,.T.);
#11288=ORIENTED_EDGE('',*,*,#8896,.T.);
#11289=ORIENTED_EDGE('',*,*,#8894,.T.);
#11290=ORIENTED_EDGE('',*,*,#8896,.F.);
#15223=CYLINDRICAL_SURFACE('',#17375,0.5);
#15224=CYLINDRICAL_SURFACE('',#17383,0.2942);
#15515=ADVANCED_FACE('',(#2205),#1659,.F.);
#15516=ADVANCED_FACE('',(#2206),#1660,.F.);
#15517=ADVANCED_FACE('',(#2207),#1661,.F.);
#15518=ADVANCED_FACE('',(#2208),#1662,.F.);
#15519=ADVANCED_FACE('',(#2209),#1663,.F.);
#15520=ADVANCED_FACE('',(#2210),#1664,.F.);
#15521=ADVANCED_FACE('',(#2211),#1665,.F.);
#15522=ADVANCED_FACE('',(#2212),#1666,.F.);
#15523=ADVANCED_FACE('',(#2213),#1667,.F.);
#15524=ADVANCED_FACE('',(#2214),#1668,.T.);
#15525=ADVANCED_FACE('',(#2215),#1025,.T.);
#15526=ADVANCED_FACE('',(#2216),#15223,.T.);
#15527=ADVANCED_FACE('',(#2217),#1026,.T.);
#15528=ADVANCED_FACE('',(#2218,#1442),#1669,.T.);
#15529=ADVANCED_FACE('',(#2219),#1027,.T.);
#15530=ADVANCED_FACE('',(#2220),#15224,.T.);
#16375=CLOSED_SHELL('',(#15515,#15516,#15517,#15518,#15519,#15520,#15521,
#15522));
#16376=CLOSED_SHELL('',(#15523,#15524,#15525,#15526,#15527,#15528,#15529,
#15530));
#17360=AXIS2_PLACEMENT_3D('',#23729,#19321,#19322);
#17361=AXIS2_PLACEMENT_3D('',#23730,#19323,#19324);
#17362=AXIS2_PLACEMENT_3D('',#23739,#19329,#19330);
#17363=AXIS2_PLACEMENT_3D('',#23745,#19334,#19335);
#17364=AXIS2_PLACEMENT_3D('',#23751,#19339,#19340);
#17365=AXIS2_PLACEMENT_3D('',#23757,#19344,#19345);
#17366=AXIS2_PLACEMENT_3D('',#23763,#19349,#19350);
#17367=AXIS2_PLACEMENT_3D('',#23766,#19353,#19354);
#17368=AXIS2_PLACEMENT_3D('',#23767,#19355,#19356);
#17369=AXIS2_PLACEMENT_3D('',#23768,#19357,#19358);
#17370=AXIS2_PLACEMENT_3D('',#23770,#19359,#19360);
#17371=AXIS2_PLACEMENT_3D('',#23771,#19361,#19362);
#17372=AXIS2_PLACEMENT_3D('',#23773,#19363,#19364);
#17373=AXIS2_PLACEMENT_3D('',#23774,#19365,#19366);
#17374=AXIS2_PLACEMENT_3D('',#23776,#19367,#19368);
#17375=AXIS2_PLACEMENT_3D('',#23778,#19370,#19371);
#17376=AXIS2_PLACEMENT_3D('',#23780,#19372,#19373);
#17377=AXIS2_PLACEMENT_3D('',#23782,#19375,#19376);
#17378=AXIS2_PLACEMENT_3D('',#23784,#19377,#19378);
#17379=AXIS2_PLACEMENT_3D('',#23786,#19380,#19381);
#17380=AXIS2_PLACEMENT_3D('',#23788,#19382,#19383);
#17381=AXIS2_PLACEMENT_3D('',#23789,#19384,#19385);
#17382=AXIS2_PLACEMENT_3D('',#23791,#19386,#19387);
#17383=AXIS2_PLACEMENT_3D('',#23793,#19389,#19390);
#19321=DIRECTION('axis',(0.,0.,1.));
#19322=DIRECTION('refdir',(1.,0.,0.));
#19323=DIRECTION('center_axis',(0.866025403784439,0.,-0.5));
#19324=DIRECTION('ref_axis',(0.5,0.,0.866025403784439));
#19325=DIRECTION('',(-0.5,0.,-0.866025403784439));
#19326=DIRECTION('',(0.,-1.,0.));
#19327=DIRECTION('',(0.5,0.,0.866025403784439));
#19328=DIRECTION('',(0.,-1.,0.));
#19329=DIRECTION('center_axis',(1.92296268638356E-16,0.,-1.));
#19330=DIRECTION('ref_axis',(1.,0.,1.92296268638356E-16));
#19331=DIRECTION('',(-1.,0.,-1.92296268638356E-16));
#19332=DIRECTION('',(0.,-1.,0.));
#19333=DIRECTION('',(1.,0.,1.92296268638356E-16));
#19334=DIRECTION('center_axis',(-0.866025403784439,0.,-0.5));
#19335=DIRECTION('ref_axis',(0.5,0.,-0.866025403784439));
#19336=DIRECTION('',(-0.5,0.,0.866025403784438));
#19337=DIRECTION('',(0.,-1.,0.));
#19338=DIRECTION('',(0.5,0.,-0.866025403784438));
#19339=DIRECTION('center_axis',(-0.866025403784439,0.,0.5));
#19340=DIRECTION('ref_axis',(-0.5,0.,-0.866025403784439));
#19341=DIRECTION('',(0.5,0.,0.866025403784439));
#19342=DIRECTION('',(0.,-1.,0.));
#19343=DIRECTION('',(-0.5,0.,-0.866025403784439));
#19344=DIRECTION('center_axis',(-1.92296268638356E-16,0.,1.));
#19345=DIRECTION('ref_axis',(-1.,0.,-1.92296268638356E-16));
#19346=DIRECTION('',(1.,0.,1.92296268638356E-16));
#19347=DIRECTION('',(0.,-1.,0.));
#19348=DIRECTION('',(-1.,0.,-1.92296268638356E-16));
#19349=DIRECTION('center_axis',(0.866025403784439,0.,0.5));
#19350=DIRECTION('ref_axis',(-0.5,0.,0.866025403784439));
#19351=DIRECTION('',(0.5,0.,-0.866025403784439));
#19352=DIRECTION('',(-0.5,0.,0.866025403784439));
#19353=DIRECTION('center_axis',(0.,1.,0.));
#19354=DIRECTION('ref_axis',(1.,0.,0.));
#19355=DIRECTION('center_axis',(0.,-1.,0.));
#19356=DIRECTION('ref_axis',(0.,0.,-1.));
#19357=DIRECTION('center_axis',(0.,1.,0.));
#19358=DIRECTION('ref_axis',(1.,0.,0.));
#19359=DIRECTION('center_axis',(0.,1.,0.));
#19360=DIRECTION('ref_axis',(1.,0.,0.));
#19361=DIRECTION('center_axis',(0.,1.,0.));
#19362=DIRECTION('ref_axis',(0.,0.,1.));
#19363=DIRECTION('center_axis',(0.,-1.,0.));
#19364=DIRECTION('ref_axis',(1.,0.,0.));
#19365=DIRECTION('center_axis',(0.,-1.,0.));
#19366=DIRECTION('ref_axis',(1.,0.,0.));
#19367=DIRECTION('center_axis',(0.,-1.,0.));
#19368=DIRECTION('ref_axis',(1.,0.,0.));
#19369=DIRECTION('',(0.707106781186548,0.707106781186547,8.65956056235494E-17));
#19370=DIRECTION('center_axis',(0.,-1.,0.));
#19371=DIRECTION('ref_axis',(1.,0.,0.));
#19372=DIRECTION('center_axis',(0.,-1.,0.));
#19373=DIRECTION('ref_axis',(1.,0.,0.));
#19374=DIRECTION('',(0.,1.,0.));
#19375=DIRECTION('center_axis',(0.,1.,0.));
#19376=DIRECTION('ref_axis',(1.,0.,0.));
#19377=DIRECTION('center_axis',(0.,-1.,0.));
#19378=DIRECTION('ref_axis',(1.,0.,0.));
#19379=DIRECTION('',(-0.707106781186547,0.707106781186548,-8.65956056235493E-17));
#19380=DIRECTION('center_axis',(0.,-1.,0.));
#19381=DIRECTION('ref_axis',(0.,0.,-1.));
#19382=DIRECTION('center_axis',(0.,-1.,0.));
#19383=DIRECTION('ref_axis',(1.,0.,0.));
#19384=DIRECTION('center_axis',(0.,1.,0.));
#19385=DIRECTION('ref_axis',(1.,0.,0.));
#19386=DIRECTION('center_axis',(0.,1.,0.));
#19387=DIRECTION('ref_axis',(1.,0.,0.));
#19388=DIRECTION('',(-0.447213595499958,0.894427190999916,-5.47678698264203E-17));
#19389=DIRECTION('center_axis',(0.,-1.,0.));
#19390=DIRECTION('ref_axis',(1.,0.,0.));
#19391=DIRECTION('',(0.,1.,0.));
#23729=CARTESIAN_POINT('',(0.,0.,0.));
#23730=CARTESIAN_POINT('Origin',(0.144337567297406,-0.6,-0.25));
#23731=CARTESIAN_POINT('',(0.288675134594813,-0.6,0.));
#23732=CARTESIAN_POINT('',(0.144337567297406,-0.6,-0.25));
#23733=CARTESIAN_POINT('',(0.288675134594813,-0.6,0.));
#23734=CARTESIAN_POINT('',(0.144337567297406,-0.96,-0.25));
#23735=CARTESIAN_POINT('',(0.144337567297406,-0.6,-0.25));
#23736=CARTESIAN_POINT('',(0.288675134594813,-0.96,0.));
#23737=CARTESIAN_POINT('',(0.288675134594813,-0.96,0.));
#23738=CARTESIAN_POINT('',(0.288675134594813,-0.6,0.));
#23739=CARTESIAN_POINT('Origin',(-0.144337567297406,-0.6,-0.25));
#23740=CARTESIAN_POINT('',(-0.144337567297406,-0.6,-0.25));
#23741=CARTESIAN_POINT('',(0.144337567297406,-0.6,-0.25));
#23742=CARTESIAN_POINT('',(-0.144337567297406,-0.96,-0.25));
#23743=CARTESIAN_POINT('',(-0.144337567297406,-0.6,-0.25));
#23744=CARTESIAN_POINT('',(0.144337567297406,-0.96,-0.25));
#23745=CARTESIAN_POINT('Origin',(-0.288675134594813,-0.6,-8.32667268468867E-17));
#23746=CARTESIAN_POINT('',(-0.288675134594813,-0.6,-3.53525079574969E-17));
#23747=CARTESIAN_POINT('',(-0.144337567297406,-0.6,-0.25));
#23748=CARTESIAN_POINT('',(-0.288675134594813,-0.96,-5.55111512312578E-17));
#23749=CARTESIAN_POINT('',(-0.288675134594813,-0.6,-3.53525079574969E-17));
#23750=CARTESIAN_POINT('',(-0.144337567297406,-0.96,-0.25));
#23751=CARTESIAN_POINT('Origin',(-0.144337567297407,-0.6,0.25));
#23752=CARTESIAN_POINT('',(-0.144337567297407,-0.6,0.25));
#23753=CARTESIAN_POINT('',(-0.288675134594813,-0.6,-3.53525079574969E-17));
#23754=CARTESIAN_POINT('',(-0.144337567297407,-0.96,0.25));
#23755=CARTESIAN_POINT('',(-0.144337567297407,-0.6,0.25));
#23756=CARTESIAN_POINT('',(-0.288675134594813,-0.96,-3.53525079574969E-17));
#23757=CARTESIAN_POINT('Origin',(0.144337567297406,-0.6,0.25));
#23758=CARTESIAN_POINT('',(0.144337567297406,-0.6,0.25));
#23759=CARTESIAN_POINT('',(-0.144337567297407,-0.6,0.25));
#23760=CARTESIAN_POINT('',(0.144337567297406,-0.96,0.25));
#23761=CARTESIAN_POINT('',(0.144337567297406,-0.6,0.25));
#23762=CARTESIAN_POINT('',(-0.144337567297407,-0.96,0.25));
#23763=CARTESIAN_POINT('Origin',(0.288675134594813,-0.6,0.));
#23764=CARTESIAN_POINT('',(0.144337567297406,-0.6,0.25));
#23765=CARTESIAN_POINT('',(0.144337567297406,-0.96,0.25));
#23766=CARTESIAN_POINT('Origin',(0.,-0.6,0.));
#23767=CARTESIAN_POINT('Origin',(0.,-0.96,0.));
#23768=CARTESIAN_POINT('Origin',(0.,-1.8,0.));
#23769=CARTESIAN_POINT('',(-0.2942,-1.8,3.60291088309151E-17));
#23770=CARTESIAN_POINT('Origin',(0.,-1.8,0.));
#23771=CARTESIAN_POINT('Origin',(0.45,0.6,0.));
#23772=CARTESIAN_POINT('',(-0.45,0.6,-5.51091059616309E-17));
#23773=CARTESIAN_POINT('Origin',(0.,0.6,0.));
#23774=CARTESIAN_POINT('Origin',(0.,0.575,0.));
#23775=CARTESIAN_POINT('',(-0.5,0.55,-6.12323399573677E-17));
#23776=CARTESIAN_POINT('Origin',(0.,0.55,0.));
#23777=CARTESIAN_POINT('',(-0.475,0.575,-5.81707229594993E-17));
#23778=CARTESIAN_POINT('Origin',(0.,0.29,0.));
#23779=CARTESIAN_POINT('',(-0.5,0.0299999999999998,-6.12323399573677E-17));
#23780=CARTESIAN_POINT('Origin',(0.,0.0299999999999998,0.));
#23781=CARTESIAN_POINT('',(-0.5,0.29,-6.12323399573677E-17));
#23782=CARTESIAN_POINT('Origin',(0.,0.0150000000000001,0.));
#23783=CARTESIAN_POINT('',(-0.47,7.11236625150491E-17,-5.75583995599256E-17));
#23784=CARTESIAN_POINT('Origin',(0.,0.,0.));
#23785=CARTESIAN_POINT('',(-0.485,0.0150000000000001,-5.93953697586466E-17));
#23786=CARTESIAN_POINT('Origin',(0.32,0.,0.));
#23787=CARTESIAN_POINT('',(-0.32,-6.93889390390723E-18,-3.91886975727153E-17));
#23788=CARTESIAN_POINT('Origin',(0.,0.,0.));
#23789=CARTESIAN_POINT('Origin',(0.,-0.02,0.));
#23790=CARTESIAN_POINT('',(-0.2942,-0.0515999999999999,3.60291088309151E-17));
#23791=CARTESIAN_POINT('Origin',(0.,-0.0515999999999999,0.));
#23792=CARTESIAN_POINT('',(-0.31,-0.02,-3.7964050773568E-17));
#23793=CARTESIAN_POINT('Origin',(0.,-1.24,0.));
#23794=CARTESIAN_POINT('',(-0.2942,-1.24,-3.60291088309151E-17));
#62619=UNCERTAINTY_MEASURE_WITH_UNIT(LENGTH_MEASURE(0.001),#62759,
'DISTANCE_ACCURACY_VALUE',
'Maximum model space distance between geometric entities at asserted c
onnectivities');
#62684=UNCERTAINTY_MEASURE_WITH_UNIT(LENGTH_MEASURE(0.001),#62759,
'DISTANCE_ACCURACY_VALUE',
'Maximum model space distance between geometric entities at asserted c
onnectivities');
#62693=(
GEOMETRIC_REPRESENTATION_CONTEXT(3)
GLOBAL_UNCERTAINTY_ASSIGNED_CONTEXT((#62619))
GLOBAL_UNIT_ASSIGNED_CONTEXT((#62759,#62761,#62762))
REPRESENTATION_CONTEXT('','3D')
);
#62758=(
GEOMETRIC_REPRESENTATION_CONTEXT(3)
GLOBAL_UNCERTAINTY_ASSIGNED_CONTEXT((#62684))
GLOBAL_UNIT_ASSIGNED_CONTEXT((#62759,#62761,#62762))
REPRESENTATION_CONTEXT('','3D')
);
#62759=(
LENGTH_UNIT()
NAMED_UNIT(*)
SI_UNIT(.CENTI.,.METRE.)
);
#62761=(
NAMED_UNIT(*)
PLANE_ANGLE_UNIT()
SI_UNIT($,.RADIAN.)
);
#62762=(
NAMED_UNIT(*)
SI_UNIT($,.STERADIAN.)
SOLID_ANGLE_UNIT()
);
#62771=SHAPE_DEFINITION_REPRESENTATION(#62844,#63039);
#62844=PRODUCT_DEFINITION_SHAPE('',$,#63113);
#63039=SHAPE_REPRESENTATION('',(#17360),#62693);
#63104=PRODUCT_DEFINITION_CONTEXT('part definition',#63325,'design');
#63113=PRODUCT_DEFINITION('M6x18 mounting screw','M6x18 mounting screw',
#63186,#63104);
#63186=PRODUCT_DEFINITION_FORMATION('',$,#63335);
#63325=APPLICATION_CONTEXT(
'Core Data for Automotive Mechanical Design Process');
#63326=PRODUCT_CONTEXT('part definition',#63325,'mechanical');
#63335=PRODUCT('M6x18 mounting screw','M6x18 mounting screw',
'M6x18 mounting screw',(#63326));
#63463=COLOUR_RGB('Black',0.12,0.14,0.17);
#63464=FILL_AREA_STYLE_COLOUR('',#63463);
#63465=FILL_AREA_STYLE('',(#63464));
#63466=SURFACE_STYLE_FILL_AREA(#63465);
#63467=SURFACE_SIDE_STYLE('',(#63466));
#63468=SURFACE_STYLE_USAGE(.BOTH.,#63467);
#63469=PRESENTATION_STYLE_ASSIGNMENT((#63468));
ENDSEC;
END-ISO-10303-21;
